ISO-10303-21;
HEADER;
FILE_DESCRIPTION((''),'2;1');
FILE_NAME('Roller Retaining Washer.step','2026-10-06T07:01:46+05:00',(''),(''),'','','');
FILE_SCHEMA (('AUTOMOTIVE_DESIGN { 1 0 10303 214 3 1 1 }'));
ENDSEC;
DATA;
#10=MECHANICAL_DESIGN_GEOMETRIC_PRESENTATION_REPRESENTATION('',(#152),#11396);
#122=SHAPE_REPRESENTATION_RELATIONSHIP('SRR','None',#11469,#137) ;
#137=ADVANCED_BREP_SHAPE_REPRESENTATION('',(#167),#11395) ;
#152=STYLED_ITEM('',(#11553),#167) ;
#167=MANIFOLD_SOLID_BREP('Roller Retaining Washer',#5583) ;
#376=FACE_BOUND('',#1217,.T.) ;
#377=FACE_BOUND('',#1220,.T.) ;
#506=PLANE('',#6389) ;
#507=PLANE('',#6393) ;
#840=FACE_OUTER_BOUND('',#1215,.T.) ;
#841=FACE_OUTER_BOUND('',#1216,.T.) ;
#842=FACE_OUTER_BOUND('',#1218,.T.) ;
#843=FACE_OUTER_BOUND('',#1219,.T.) ;
#1215=EDGE_LOOP('',(#5080,#5081,#5082,#5083)) ;
#1216=EDGE_LOOP('',(#5084)) ;
#1217=EDGE_LOOP('',(#5085)) ;
#1218=EDGE_LOOP('',(#5086,#5087,#5088,#5089)) ;
#1219=EDGE_LOOP('',(#5090)) ;
#1220=EDGE_LOOP('',(#5091)) ;
#1602=LINE('',#11332,#1985) ;
#1603=LINE('',#11340,#1986) ;
#1985=VECTOR('',#8072,1.525) ;
#1986=VECTOR('',#8083,2.225) ;
#2265=CIRCLE('',#6387,1.525) ;
#2266=CIRCLE('',#6388,1.525) ;
#2267=CIRCLE('',#6390,2.225) ;
#2268=CIRCLE('',#6392,2.225) ;
#2742=VERTEX_POINT('',#11329) ;
#2743=VERTEX_POINT('',#11331) ;
#2744=VERTEX_POINT('',#11335) ;
#2745=VERTEX_POINT('',#11338) ;
#3522=EDGE_CURVE('',#2742,#2742,#2265,.T.) ;
#3523=EDGE_CURVE('',#2742,#2743,#1602,.T.) ;
#3524=EDGE_CURVE('',#2743,#2743,#2266,.T.) ;
#3525=EDGE_CURVE('',#2744,#2744,#2267,.T.) ;
#3526=EDGE_CURVE('',#2745,#2745,#2268,.T.) ;
#3527=EDGE_CURVE('',#2745,#2744,#1603,.T.) ;
#5080=ORIENTED_EDGE('',*,*,#3522,.T.) ;
#5081=ORIENTED_EDGE('',*,*,#3523,.T.) ;
#5082=ORIENTED_EDGE('',*,*,#3524,.F.) ;
#5083=ORIENTED_EDGE('',*,*,#3523,.F.) ;
#5084=ORIENTED_EDGE('',*,*,#3525,.F.) ;
#5085=ORIENTED_EDGE('',*,*,#3524,.T.) ;
#5086=ORIENTED_EDGE('',*,*,#3526,.F.) ;
#5087=ORIENTED_EDGE('',*,*,#3527,.T.) ;
#5088=ORIENTED_EDGE('',*,*,#3525,.T.) ;
#5089=ORIENTED_EDGE('',*,*,#3527,.F.) ;
#5090=ORIENTED_EDGE('',*,*,#3526,.T.) ;
#5091=ORIENTED_EDGE('',*,*,#3522,.F.) ;
#5231=CYLINDRICAL_SURFACE('',#6386,1.525) ;
#5232=CYLINDRICAL_SURFACE('',#6391,2.225) ;
#5565=ADVANCED_FACE('',(#840),#5231,.F.) ;
#5566=ADVANCED_FACE('',(#841,#376),#506,.T.) ;
#5567=ADVANCED_FACE('',(#842),#5232,.T.) ;
#5568=ADVANCED_FACE('',(#843,#377),#507,.T.) ;
#5583=CLOSED_SHELL('',(#5565,#5566,#5567,#5568)) ;
#6385=AXIS2_PLACEMENT_3D('',#11327,#8066,#8067) ;
#6386=AXIS2_PLACEMENT_3D('',#11328,#8068,#8069) ;
#6387=AXIS2_PLACEMENT_3D('',#11330,#8070,#8071) ;
#6388=AXIS2_PLACEMENT_3D('',#11333,#8073,#8074) ;
#6389=AXIS2_PLACEMENT_3D('',#11334,#8075,#8076) ;
#6390=AXIS2_PLACEMENT_3D('',#11336,#8077,#8078) ;
#6391=AXIS2_PLACEMENT_3D('',#11337,#8079,#8080) ;
#6392=AXIS2_PLACEMENT_3D('',#11339,#8081,#8082) ;
#6393=AXIS2_PLACEMENT_3D('',#11341,#8084,#8085) ;
#8066=DIRECTION('axis',(0.,0.,1.)) ;
#8067=DIRECTION('refdir',(1.,0.,0.)) ;
#8068=DIRECTION('center_axis',(1.,0.,0.)) ;
#8069=DIRECTION('ref_axis',(0.,1.,0.)) ;
#8070=DIRECTION('center_axis',(1.,0.,0.)) ;
#8071=DIRECTION('ref_axis',(0.,0.,-1.)) ;
#8072=DIRECTION('',(-1.,0.,0.)) ;
#8073=DIRECTION('center_axis',(1.,0.,0.)) ;
#8074=DIRECTION('ref_axis',(0.,0.,-1.)) ;
#8075=DIRECTION('center_axis',(-1.,0.,0.)) ;
#8076=DIRECTION('ref_axis',(0.,0.,1.)) ;
#8077=DIRECTION('center_axis',(1.,0.,0.)) ;
#8078=DIRECTION('ref_axis',(0.,0.,-1.)) ;
#8079=DIRECTION('center_axis',(1.,0.,0.)) ;
#8080=DIRECTION('ref_axis',(0.,1.,0.)) ;
#8081=DIRECTION('center_axis',(1.,0.,0.)) ;
#8082=DIRECTION('ref_axis',(0.,0.,-1.)) ;
#8083=DIRECTION('',(-1.,0.,0.)) ;
#8084=DIRECTION('center_axis',(1.,0.,0.)) ;
#8085=DIRECTION('ref_axis',(0.,0.,-1.)) ;
#11327=CARTESIAN_POINT('',(0.,0.,0.)) ;
#11328=CARTESIAN_POINT('Origin',(6.425,19.79,38.695)) ;
#11329=CARTESIAN_POINT('',(6.585,18.265,38.695)) ;
#11330=CARTESIAN_POINT('Origin',(6.585,19.79,38.695)) ;
#11331=CARTESIAN_POINT('',(6.265,18.265,38.695)) ;
#11332=CARTESIAN_POINT('',(6.425,18.265,38.695)) ;
#11333=CARTESIAN_POINT('Origin',(6.265,19.79,38.695)) ;
#11334=CARTESIAN_POINT('Origin',(6.265,22.015,38.695)) ;
#11335=CARTESIAN_POINT('',(6.265,17.565,38.695)) ;
#11336=CARTESIAN_POINT('Origin',(6.265,19.79,38.695)) ;
#11337=CARTESIAN_POINT('Origin',(6.425,19.79,38.695)) ;
#11338=CARTESIAN_POINT('',(6.585,17.565,38.695)) ;
#11339=CARTESIAN_POINT('Origin',(6.585,19.79,38.695)) ;
#11340=CARTESIAN_POINT('',(6.425,17.565,38.695)) ;
#11341=CARTESIAN_POINT('Origin',(6.585,21.315,38.695)) ;
#11378=UNCERTAINTY_MEASURE_WITH_UNIT(LENGTH_MEASURE(0.01),#11397,
'DISTANCE_ACCURACY_VALUE',
'Maximum model space distance between geometric entities at asserted c
onnectivities') ;
#11379=UNCERTAINTY_MEASURE_WITH_UNIT(LENGTH_MEASURE(0.01),#11397,
'DISTANCE_ACCURACY_VALUE',
'Maximum model space distance between geometric entities at asserted c
onnectivities') ;
#11395=(
GEOMETRIC_REPRESENTATION_CONTEXT(3)
GLOBAL_UNCERTAINTY_ASSIGNED_CONTEXT((#11378))
GLOBAL_UNIT_ASSIGNED_CONTEXT((#11397,#11399,#11400))
REPRESENTATION_CONTEXT('','3D')
) ;
#11396=(
GEOMETRIC_REPRESENTATION_CONTEXT(3)
GLOBAL_UNCERTAINTY_ASSIGNED_CONTEXT((#11379))
GLOBAL_UNIT_ASSIGNED_CONTEXT((#11397,#11399,#11400))
REPRESENTATION_CONTEXT('','3D')
) ;
#11397=(
LENGTH_UNIT()
NAMED_UNIT(*)
SI_UNIT(.MILLI.,.METRE.)
) ;
#11399=(
NAMED_UNIT(*)
PLANE_ANGLE_UNIT()
SI_UNIT($,.RADIAN.)
) ;
#11400=(
NAMED_UNIT(*)
SI_UNIT($,.STERADIAN.)
SOLID_ANGLE_UNIT()
) ;
#11416=SHAPE_DEFINITION_REPRESENTATION(#11432,#11469) ;
#11432=PRODUCT_DEFINITION_SHAPE('',$,#11486) ;
#11469=SHAPE_REPRESENTATION('',(#6385),#11395) ;
#11470=PRODUCT_DEFINITION_CONTEXT('part definition',#11520,'design') ;
#11486=PRODUCT_DEFINITION('Roller Retaining Washer',
'Roller Retaining Washer',#11502,#11470) ;
#11502=PRODUCT_DEFINITION_FORMATION('',$,#11537) ;
#11520=APPLICATION_CONTEXT(
'Core Data for Automotive Mechanical Design Process') ;
#11521=PRODUCT_CONTEXT('part definition',#11520,'mechanical') ;
#11537=PRODUCT('Roller Retaining Washer','Roller Retaining Washer',$,(#11521)) ;
#11553=PRESENTATION_STYLE_ASSIGNMENT((#11569)) ;
#11569=SURFACE_STYLE_USAGE(.BOTH.,#11585) ;
#11585=SURFACE_SIDE_STYLE('',(#11601)) ;
#11601=SURFACE_STYLE_FILL_AREA(#11617) ;
#11617=FILL_AREA_STYLE('MAS-252 Metallic - Roller Retaining Washer',(#11633)) ;
#11633=FILL_AREA_STYLE_COLOUR(
'MAS-252 Metallic - Roller Retaining Washer',#11649) ;
#11649=COLOUR_RGB('MAS-252 Metallic - Roller Retaining Washer', 0.31764706, 0.68627451, 0.89019608) ;
ENDSEC;
END-ISO-10303-21;
